ISO-10303-21;
HEADER;
FILE_DESCRIPTION (('STEP AP203'),
    '1' );
FILE_NAME ('1602p_c_06.step',
    '2026-10-31T14:11:27',
    ( '' ),
    ( '' ),
    'SwSTEP 2.0',
    'SolidWorks 2024',
    '' );
FILE_SCHEMA (( 'AUTOMOTIVE_DESIGN' ));
ENDSEC;

DATA;
#261=ORIENTED_EDGE ( 'NONE', *, *, #549, .T. ) ;
#352=EDGE_CURVE ( 'NONE', #17009, #12811, #11602, .T. ) ;
#415=DIRECTION ( 'NONE',  ( 1.000000000000000000, 0.000000000000000000, 0.000000000000000000 ) ) ;
#549=EDGE_CURVE ( 'NONE', #20086, #18306, #5988, .T. ) ;
#559=LINE ( 'NONE', #17060, #5451 ) ;
#825=CARTESIAN_POINT ( 'NONE',  ( -16.50000000000000000, -20.00000000000000000, -2.500000000000000000 ) ) ;
#966=ORIENTED_EDGE ( 'NONE', *, *, #9719, .T. ) ;
#1229=DIRECTION ( 'NONE',  ( 0.000000000000000000, 0.000000000000000000, -1.000000000000000000 ) ) ;
#1317=AXIS2_PLACEMENT_3D ( 'NONE', #19326, #4958, #7734 ) ;
#1321=ORIENTED_EDGE ( 'NONE', *, *, #8670, .F. ) ;
#1512=CARTESIAN_POINT ( 'NONE',  ( -16.50000000000000000, -20.00000000000000000, 2.500000000000000000 ) ) ;
#1534=FACE_OUTER_BOUND ( 'NONE', #19911, .T. ) ;
#1601=EDGE_LOOP ( 'NONE', ( #17670, #11463 ) ) ;
#1611=CIRCLE ( 'NONE', #16790, 3.499999999999999556 ) ;
#1612=FACE_OUTER_BOUND ( 'NONE', #3859, .T. ) ;
#1690=APPLICATION_CONTEXT ( 'configuration controlled 3d designs of mechanical parts and assemblies' ) ;
#1893=ORIENTED_EDGE ( 'NONE', *, *, #9719, .F. ) ;
#1957=VERTEX_POINT ( 'NONE', #825 ) ;
#2112=VERTEX_POINT ( 'NONE', #13899 ) ;
#2273=VECTOR ( 'NONE', #5849, 1000.000000000000000 ) ;
#2471=CARTESIAN_POINT ( 'NONE',  ( -25.00000000000000000, -20.00000000000000000, -2.500000000000000000 ) ) ;
#2569=CARTESIAN_POINT ( 'NONE',  ( 0.000000000000000000, 0.000000000000000000, 0.000000000000000000 ) ) ;
#2601=EDGE_LOOP ( 'NONE', ( #3077, #13801 ) ) ;
#2785=VECTOR ( 'NONE', #12259, 1000.000000000000000 ) ;
#3077=ORIENTED_EDGE ( 'NONE', *, *, #21436, .T. ) ;
#3438=CARTESIAN_POINT ( 'NONE',  ( -20.00000000000000000, -20.00000000000000000, 2.500000000000000000 ) ) ;
#3550=DIRECTION ( 'NONE',  ( 0.000000000000000000, 0.000000000000000000, -1.000000000000000000 ) ) ;
#3574=CARTESIAN_POINT ( 'NONE',  ( -20.00000000000000000, -20.00000000000000000, 0.000000000000000000 ) ) ;
#3704=DIRECTION ( 'NONE',  ( 0.000000000000000000, 0.000000000000000000, -1.000000000000000000 ) ) ;
#3859=EDGE_LOOP ( 'NONE', ( #17470, #16589 ) ) ;
#3949=AXIS2_PLACEMENT_3D ( 'NONE', #21656, #8975, #14661 ) ;
#3996=APPLICATION_CONTEXT ( 'configuration controlled 3d designs of mechanical parts and assemblies' ) ;
#4148=EDGE_CURVE ( 'NONE', #1957, #12690, #1611, .T. ) ;
#4322=ORIENTED_EDGE ( 'NONE', *, *, #5625, .F. ) ;
#4488=ORIENTED_EDGE ( 'NONE', *, *, #7740, .T. ) ;
#4515=VECTOR ( 'NONE', #1229, 1000.000000000000000 ) ;
#4682=CARTESIAN_POINT ( 'NONE',  ( -23.50000000000000000, -20.00000000000000000, -2.500000000000000000 ) ) ;
#4816=( NAMED_UNIT ( * ) PLANE_ANGLE_UNIT ( ) SI_UNIT ( $, .RADIAN. ) );
#4835=CARTESIAN_POINT ( 'NONE',  ( -20.00000000000000000, -20.00000000000000000, -2.500000000000000000 ) ) ;
#4958=DIRECTION ( 'NONE',  ( 0.000000000000000000, 0.000000000000000000, -1.000000000000000000 ) ) ;
#5100=ORIENTED_EDGE ( 'NONE', *, *, #8670, .T. ) ;
#5149=DIRECTION ( 'NONE',  ( 0.000000000000000000, 0.000000000000000000, 1.000000000000000000 ) ) ;
#5451=VECTOR ( 'NONE', #15286, 1000.000000000000000 ) ;
#5625=EDGE_CURVE ( 'NONE', #17009, #1957, #11615, .T. ) ;
#5849=DIRECTION ( 'NONE',  ( 0.000000000000000000, 0.000000000000000000, -1.000000000000000000 ) ) ;
#5946=CIRCLE ( 'NONE', #6339, 5.000000000000000888 ) ;
#5988=CIRCLE ( 'NONE', #16232, 5.000000000000000888 ) ;
#6090=ORIENTED_EDGE ( 'NONE', *, *, #21436, .F. ) ;
#6259=ADVANCED_BREP_SHAPE_REPRESENTATION ( '', ( #17099, #12739 ), #9323 ) ;
#6303=EDGE_CURVE ( 'NONE', #18306, #20086, #23267, .T. ) ;
#6339=AXIS2_PLACEMENT_3D ( 'NONE', #16677, #13031, #22379 ) ;
#6478=( LENGTH_UNIT ( ) NAMED_UNIT ( * ) SI_UNIT ( .MILLI., .METRE. ) );
#6598=CARTESIAN_POINT ( 'NONE',  ( -20.00000000000000000, -20.00000000000000000, -2.500000000000000000 ) ) ;
#6753=SHAPE_DEFINITION_REPRESENTATION ( #15381, #11141 ) ;
#6907=ORIENTED_EDGE ( 'NONE', *, *, #6303, .T. ) ;
#7612=CARTESIAN_POINT ( 'NONE',  ( -20.00000000000000000, -20.00000000000000000, -2.500000000000000000 ) ) ;
#7667=EDGE_CURVE ( 'NONE', #2112, #20086, #8449, .T. ) ;
#7717=CIRCLE ( 'NONE', #11921, 3.499999999999999556 ) ;
#7734=DIRECTION ( 'NONE',  ( -1.000000000000000000, 0.000000000000000000, 0.000000000000000000 ) ) ;
#7740=EDGE_CURVE ( 'NONE', #9304, #2112, #15687, .T. ) ;
#7821=MECHANICAL_CONTEXT ( 'NONE', #1690, 'mechanical' ) ;
#8087=ORIENTED_EDGE ( 'NONE', *, *, #18381, .T. ) ;
#8101=ADVANCED_FACE ( 'NONE', ( #22766 ), #20649, .T. ) ;
#8449=LINE ( 'NONE', #19710, #2785 ) ;
#8470=DIRECTION ( 'NONE',  ( 0.000000000000000000, 0.000000000000000000, 1.000000000000000000 ) ) ;
#8572=DIRECTION ( 'NONE',  ( 0.000000000000000000, 0.000000000000000000, -1.000000000000000000 ) ) ;
#8670=EDGE_CURVE ( 'NONE', #12811, #17009, #7717, .T. ) ;
#8710=CARTESIAN_POINT ( 'NONE',  ( -23.50000000000000000, -20.00000000000000000, 2.500000000000000000 ) ) ;
#8757=DIRECTION ( 'NONE',  ( -1.000000000000000000, 0.000000000000000000, 0.000000000000000000 ) ) ;
#8803=DIRECTION ( 'NONE',  ( -1.000000000000000000, 0.000000000000000000, 0.000000000000000000 ) ) ;
#8941=ADVANCED_FACE ( 'NONE', ( #11002 ), #18229, .T. ) ;
#8975=DIRECTION ( 'NONE',  ( 0.000000000000000000, 0.000000000000000000, -1.000000000000000000 ) ) ;
#8997=CARTESIAN_POINT ( 'NONE',  ( -20.00000000000000000, -20.00000000000000000, -2.500000000000000000 ) ) ;
#9044=EDGE_LOOP ( 'NONE', ( #15923, #16553, #6090, #21098 ) ) ;
#9304=VERTEX_POINT ( 'NONE', #10400 ) ;
#9323=( GEOMETRIC_REPRESENTATION_CONTEXT ( 3 ) GLOBAL_UNCERTAINTY_ASSIGNED_CONTEXT ( ( #21770 ) ) GLOBAL_UNIT_ASSIGNED_CONTEXT ( ( #6478, #4816, #19894 ) ) REPRESENTATION_CONTEXT ( 'NONE', 'WORKASPACE' ) );
#9456=ADVANCED_FACE ( 'NONE', ( #18328 ), #19980, .F. ) ;
#9719=EDGE_CURVE ( 'NONE', #9304, #18306, #16632, .T. ) ;
#9968=ADVANCED_FACE ( 'NONE', ( #1534 ), #12604, .F. ) ;
#10167=DIRECTION ( 'NONE',  ( -1.000000000000000000, 0.000000000000000000, 0.000000000000000000 ) ) ;
#10289=AXIS2_PLACEMENT_3D ( 'NONE', #3574, #10597, #8803 ) ;
#10363=DIRECTION ( 'NONE',  ( -1.000000000000000000, 0.000000000000000000, 0.000000000000000000 ) ) ;
#10400=CARTESIAN_POINT ( 'NONE',  ( -25.00000000000000000, -20.00000000000000000, 2.500000000000000000 ) ) ;
#10401=AXIS2_PLACEMENT_3D ( 'NONE', #13815, #8470, #12389 ) ;
#10597=DIRECTION ( 'NONE',  ( 0.000000000000000000, 0.000000000000000000, -1.000000000000000000 ) ) ;
#10669=FACE_BOUND ( 'NONE', #2601, .T. ) ;
#11002=FACE_OUTER_BOUND ( 'NONE', #13778, .T. ) ;
#11141=SHAPE_REPRESENTATION ( '1602p_c_06', ( #12739 ), #9323 ) ;
#11463=ORIENTED_EDGE ( 'NONE', *, *, #21947, .F. ) ;
#11512=DIRECTION ( 'NONE',  ( -1.000000000000000000, 0.000000000000000000, 0.000000000000000000 ) ) ;
#11602=CIRCLE ( 'NONE', #1317, 3.499999999999999556 ) ;
#11615=LINE ( 'NONE', #22505, #4515 ) ;
#11921=AXIS2_PLACEMENT_3D ( 'NONE', #15387, #22620, #11512 ) ;
#12259=DIRECTION ( 'NONE',  ( 0.000000000000000000, 0.000000000000000000, -1.000000000000000000 ) ) ;
#12389=DIRECTION ( 'NONE',  ( -1.000000000000000000, 0.000000000000000000, 0.000000000000000000 ) ) ;
#12443=CARTESIAN_POINT ( 'NONE',  ( -15.00000000000000000, -20.00000000000000000, -2.500000000000000000 ) ) ;
#12581=FACE_BOUND ( 'NONE', #16327, .T. ) ;
#12604=CYLINDRICAL_SURFACE ( 'NONE', #10289, 3.499999999999999556 ) ;
#12690=VERTEX_POINT ( 'NONE', #4682 ) ;
#12739=AXIS2_PLACEMENT_3D ( 'NONE', #2569, #13380, #415 ) ;
#12811=VERTEX_POINT ( 'NONE', #8710 ) ;
#13031=DIRECTION ( 'NONE',  ( 0.000000000000000000, 0.000000000000000000, -1.000000000000000000 ) ) ;
#13090=DIRECTION ( 'NONE',  ( 0.000000000000000000, 0.000000000000000000, 1.000000000000000000 ) ) ;
#13292=PRODUCT ( '1602p_c_06', '1602p_c_06', '', ( #7821 ) ) ;
#13373=AXIS2_PLACEMENT_3D ( 'NONE', #4835, #16112, #22991 ) ;
#13380=DIRECTION ( 'NONE',  ( 0.000000000000000000, 0.000000000000000000, 1.000000000000000000 ) ) ;
#13524=CIRCLE ( 'NONE', #23359, 3.499999999999999556 ) ;
#13778=EDGE_LOOP ( 'NONE', ( #14466, #17449, #966, #6907 ) ) ;
#13801=ORIENTED_EDGE ( 'NONE', *, *, #4148, .T. ) ;
#13815=CARTESIAN_POINT ( 'NONE',  ( -20.00000000000000000, -20.00000000000000000, -2.500000000000000000 ) ) ;
#13899=CARTESIAN_POINT ( 'NONE',  ( -15.00000000000000000, -20.00000000000000000, 2.500000000000000000 ) ) ;
#14234=FACE_OUTER_BOUND ( 'NONE', #1601, .T. ) ;
#14328=PLANE ( 'NONE',  #13373 ) ;
#14351=CARTESIAN_POINT ( 'NONE',  ( -20.00000000000000000, -20.00000000000000000, 2.500000000000000000 ) ) ;
#14356=ORIENTED_EDGE ( 'NONE', *, *, #352, .T. ) ;
#14466=ORIENTED_EDGE ( 'NONE', *, *, #7667, .F. ) ;
#14532=AXIS2_PLACEMENT_3D ( 'NONE', #20416, #15532, #19118 ) ;
#14661=DIRECTION ( 'NONE',  ( -1.000000000000000000, 0.000000000000000000, 0.000000000000000000 ) ) ;
#14861=CARTESIAN_POINT ( 'NONE',  ( -25.00000000000000000, -20.00000000000000000, 0.000000000000000000 ) ) ;
#14948=ORIENTED_EDGE ( 'NONE', *, *, #7667, .T. ) ;
#15286=DIRECTION ( 'NONE',  ( 0.000000000000000000, 0.000000000000000000, -1.000000000000000000 ) ) ;
#15381=PRODUCT_DEFINITION_SHAPE ( 'NONE', 'NONE',  #17062 ) ;
#15387=CARTESIAN_POINT ( 'NONE',  ( -20.00000000000000000, -20.00000000000000000, 2.500000000000000000 ) ) ;
#15532=DIRECTION ( 'NONE',  ( 0.000000000000000000, 0.000000000000000000, -1.000000000000000000 ) ) ;
#15652=PRODUCT_DEFINITION_FORMATION_WITH_SPECIFIED_SOURCE ( 'ANY', '', #13292, .NOT_KNOWN. ) ;
#15687=CIRCLE ( 'NONE', #18739, 5.000000000000000888 ) ;
#15923=ORIENTED_EDGE ( 'NONE', *, *, #352, .F. ) ;
#16112=DIRECTION ( 'NONE',  ( 0.000000000000000000, 0.000000000000000000, -1.000000000000000000 ) ) ;
#16178=CARTESIAN_POINT ( 'NONE',  ( -20.00000000000000000, -20.00000000000000000, 0.000000000000000000 ) ) ;
#16232=AXIS2_PLACEMENT_3D ( 'NONE', #8997, #16336, #8757 ) ;
#16327=EDGE_LOOP ( 'NONE', ( #5100, #14356 ) ) ;
#16336=DIRECTION ( 'NONE',  ( 0.000000000000000000, 0.000000000000000000, 1.000000000000000000 ) ) ;
#16553=ORIENTED_EDGE ( 'NONE', *, *, #5625, .T. ) ;
#16589=ORIENTED_EDGE ( 'NONE', *, *, #549, .F. ) ;
#16632=LINE ( 'NONE', #14861, #2273 ) ;
#16677=CARTESIAN_POINT ( 'NONE',  ( -20.00000000000000000, -20.00000000000000000, 2.500000000000000000 ) ) ;
#16790=AXIS2_PLACEMENT_3D ( 'NONE', #6598, #5149, #10167 ) ;
#17009=VERTEX_POINT ( 'NONE', #1512 ) ;
#17060=CARTESIAN_POINT ( 'NONE',  ( -23.50000000000000000, -20.00000000000000000, 0.000000000000000000 ) ) ;
#17062=PRODUCT_DEFINITION ( 'UNKNOWN', '', #15652, #22978 ) ;
#17099=MANIFOLD_SOLID_BREP ( 'Imported1', #20812 ) ;
#17449=ORIENTED_EDGE ( 'NONE', *, *, #21947, .T. ) ;
#17470=ORIENTED_EDGE ( 'NONE', *, *, #6303, .F. ) ;
#17670=ORIENTED_EDGE ( 'NONE', *, *, #7740, .F. ) ;
#18002=ADVANCED_FACE ( 'NONE', ( #12581, #14234 ), #21363, .F. ) ;
#18198=DIRECTION ( 'NONE',  ( -1.000000000000000000, 0.000000000000000000, 0.000000000000000000 ) ) ;
#18220=AXIS2_PLACEMENT_3D ( 'NONE', #16178, #3704, #18198 ) ;
#18229=CYLINDRICAL_SURFACE ( 'NONE', #3949, 5.000000000000000888 ) ;
#18306=VERTEX_POINT ( 'NONE', #2471 ) ;
#18328=FACE_OUTER_BOUND ( 'NONE', #9044, .T. ) ;
#18381=EDGE_CURVE ( 'NONE', #12811, #12690, #559, .T. ) ;
#18739=AXIS2_PLACEMENT_3D ( 'NONE', #3438, #8572, #10363 ) ;
#19118=DIRECTION ( 'NONE',  ( -1.000000000000000000, 0.000000000000000000, 0.000000000000000000 ) ) ;
#19326=CARTESIAN_POINT ( 'NONE',  ( -20.00000000000000000, -20.00000000000000000, 2.500000000000000000 ) ) ;
#19538=SHAPE_REPRESENTATION_RELATIONSHIP ( 'NONE' , 'NONE' ,  #11141, #6259 ) ;
#19710=CARTESIAN_POINT ( 'NONE',  ( -15.00000000000000000, -20.00000000000000000, 0.000000000000000000 ) ) ;
#19894=( NAMED_UNIT ( * ) SI_UNIT ( $, .STERADIAN. ) SOLID_ANGLE_UNIT ( ) );
#19911=EDGE_LOOP ( 'NONE', ( #4322, #1321, #8087, #21647 ) ) ;
#19980=CYLINDRICAL_SURFACE ( 'NONE', #18220, 3.499999999999999556 ) ;
#20026=ADVANCED_FACE ( 'NONE', ( #10669, #1612 ), #14328, .T. ) ;
#20086=VERTEX_POINT ( 'NONE', #12443 ) ;
#20322=DIRECTION ( 'NONE',  ( -1.000000000000000000, 0.000000000000000000, 0.000000000000000000 ) ) ;
#20416=CARTESIAN_POINT ( 'NONE',  ( -20.00000000000000000, -20.00000000000000000, 0.000000000000000000 ) ) ;
#20421=EDGE_LOOP ( 'NONE', ( #4488, #14948, #261, #1893 ) ) ;
#20649=CYLINDRICAL_SURFACE ( 'NONE', #14532, 5.000000000000000888 ) ;
#20812=CLOSED_SHELL ( 'NONE', ( #8101, #9456, #9968, #18002, #8941, #20026 ) ) ;
#21098=ORIENTED_EDGE ( 'NONE', *, *, #18381, .F. ) ;
#21363=PLANE ( 'NONE',  #21402 ) ;
#21402=AXIS2_PLACEMENT_3D ( 'NONE', #14351, #3550, #23011 ) ;
#21436=EDGE_CURVE ( 'NONE', #12690, #1957, #13524, .T. ) ;
#21647=ORIENTED_EDGE ( 'NONE', *, *, #4148, .F. ) ;
#21656=CARTESIAN_POINT ( 'NONE',  ( -20.00000000000000000, -20.00000000000000000, 0.000000000000000000 ) ) ;
#21770=UNCERTAINTY_MEASURE_WITH_UNIT (LENGTH_MEASURE( 1.000000000000000082E-05 ), #6478, 'distance_accuracy_value', 'NONE');
#21947=EDGE_CURVE ( 'NONE', #2112, #9304, #5946, .T. ) ;
#22379=DIRECTION ( 'NONE',  ( -1.000000000000000000, 0.000000000000000000, 0.000000000000000000 ) ) ;
#22505=CARTESIAN_POINT ( 'NONE',  ( -16.50000000000000000, -20.00000000000000000, 0.000000000000000000 ) ) ;
#22620=DIRECTION ( 'NONE',  ( 0.000000000000000000, 0.000000000000000000, -1.000000000000000000 ) ) ;
#22766=FACE_OUTER_BOUND ( 'NONE', #20421, .T. ) ;
#22978=DESIGN_CONTEXT ( 'detailed design', #3996, 'design' ) ;
#22991=DIRECTION ( 'NONE',  ( 0.000000000000000000, -1.000000000000000000, 0.000000000000000000 ) ) ;
#23011=DIRECTION ( 'NONE',  ( 0.000000000000000000, -1.000000000000000000, 0.000000000000000000 ) ) ;
#23267=CIRCLE ( 'NONE', #10401, 5.000000000000000888 ) ;
#23359=AXIS2_PLACEMENT_3D ( 'NONE', #7612, #13090, #20322 ) ;
#23550=COLOUR_RGB('Black', 0.08235294, 0.09019608, 0.10196078);
#23551=FILL_AREA_STYLE_COLOUR('',#23550);
#23552=FILL_AREA_STYLE('',(#23551));
#23553=SURFACE_STYLE_FILL_AREA(#23552);
#23554=SURFACE_SIDE_STYLE('',(#23553));
#23555=SURFACE_STYLE_USAGE(.BOTH.,#23554);
#23556=PRESENTATION_STYLE_ASSIGNMENT((#23555));
#23577=STYLED_ITEM('',(#23556),#17099);
#23578=MECHANICAL_DESIGN_GEOMETRIC_PRESENTATION_REPRESENTATION('',(#23577),#9323);
ENDSEC;
END-ISO-10303-21;
